ISO-10303-21;
HEADER;
/* Generated by software containing ST-Developer
 * from STEP Tools, Inc. (www.steptools.com) 
 */

FILE_DESCRIPTION(
/* description */ (''),
/* implementation_level */ '2;1');

FILE_NAME(
/* name */ 'Rail_02.step',
/* time_stamp */ '2026-10-19T01:17:59+06:00',
/* author */ (''),
/* organization */ (''),
/* preprocessor_version */ 'ST-DEVELOPER v20.2',
/* originating_system */ 'Autodesk Translation Framework v15.15.0.0',
/* authorisation */ '');

FILE_SCHEMA (('AUTOMOTIVE_DESIGN { 1 0 10303 214 3 1 1 }'));
ENDSEC;

DATA;
#10=MECHANICAL_DESIGN_GEOMETRIC_PRESENTATION_REPRESENTATION('',(#750),#48369);
#619=SHAPE_REPRESENTATION_RELATIONSHIP('SRR','None',#48419,#630);
#630=ADVANCED_BREP_SHAPE_REPRESENTATION('',(#776),#48364);
#750=STYLED_ITEM('',(#48531),#776);
#776=MANIFOLD_SOLID_BREP('Rail_02',#20129);
#1168=CYLINDRICAL_SURFACE('',#21738,0.450000000000145);
#1169=CYLINDRICAL_SURFACE('',#21741,2.46743797397102);
#1170=CYLINDRICAL_SURFACE('',#21744,0.725000000000007);
#1171=CYLINDRICAL_SURFACE('',#21748,0.599999999999981);
#1172=CYLINDRICAL_SURFACE('',#21751,2.3640229247478);
#1173=CYLINDRICAL_SURFACE('',#21754,1.39999999999995);
#1174=CYLINDRICAL_SURFACE('',#21758,1.05000000000001);
#1175=CYLINDRICAL_SURFACE('',#21762,1.04999999999996);
#1176=CYLINDRICAL_SURFACE('',#21766,1.09999999999999);
#1177=CYLINDRICAL_SURFACE('',#21782,0.450000000000145);
#1178=CYLINDRICAL_SURFACE('',#21784,2.46743797397102);
#1179=CYLINDRICAL_SURFACE('',#21786,0.725000000000007);
#1180=CYLINDRICAL_SURFACE('',#21789,0.599999999999981);
#1181=CYLINDRICAL_SURFACE('',#21791,2.3640229247478);
#1182=CYLINDRICAL_SURFACE('',#21793,1.39999999999995);
#1183=CYLINDRICAL_SURFACE('',#21796,1.05000000000001);
#1184=CYLINDRICAL_SURFACE('',#21799,1.04999999999996);
#1185=CYLINDRICAL_SURFACE('',#21802,1.09999999999999);
#2158=FACE_OUTER_BOUND('',#3290,.T.);
#2159=FACE_OUTER_BOUND('',#3291,.T.);
#2160=FACE_OUTER_BOUND('',#3292,.T.);
#2161=FACE_OUTER_BOUND('',#3293,.T.);
#2162=FACE_OUTER_BOUND('',#3294,.T.);
#2163=FACE_OUTER_BOUND('',#3295,.T.);
#2164=FACE_OUTER_BOUND('',#3296,.T.);
#2165=FACE_OUTER_BOUND('',#3297,.T.);
#2166=FACE_OUTER_BOUND('',#3298,.T.);
#2167=FACE_OUTER_BOUND('',#3299,.T.);
#2168=FACE_OUTER_BOUND('',#3300,.T.);
#2169=FACE_OUTER_BOUND('',#3301,.T.);
#2170=FACE_OUTER_BOUND('',#3302,.T.);
#2171=FACE_OUTER_BOUND('',#3303,.T.);
#2172=FACE_OUTER_BOUND('',#3304,.T.);
#2173=FACE_OUTER_BOUND('',#3305,.T.);
#2174=FACE_OUTER_BOUND('',#3306,.T.);
#2175=FACE_OUTER_BOUND('',#3307,.T.);
#2176=FACE_OUTER_BOUND('',#3308,.T.);
#2177=FACE_OUTER_BOUND('',#3309,.T.);
#2178=FACE_OUTER_BOUND('',#3310,.T.);
#2179=FACE_OUTER_BOUND('',#3311,.T.);
#2180=FACE_OUTER_BOUND('',#3312,.T.);
#2181=FACE_OUTER_BOUND('',#3313,.T.);
#2182=FACE_OUTER_BOUND('',#3314,.T.);
#2183=FACE_OUTER_BOUND('',#3315,.T.);
#2184=FACE_OUTER_BOUND('',#3316,.T.);
#2185=FACE_OUTER_BOUND('',#3317,.T.);
#2186=FACE_OUTER_BOUND('',#3318,.T.);
#2187=FACE_OUTER_BOUND('',#3319,.T.);
#2188=FACE_OUTER_BOUND('',#3320,.T.);
#2189=FACE_OUTER_BOUND('',#3321,.T.);
#2190=FACE_OUTER_BOUND('',#3322,.T.);
#2191=FACE_OUTER_BOUND('',#3323,.T.);
#2192=FACE_OUTER_BOUND('',#3324,.T.);
#2193=FACE_OUTER_BOUND('',#3325,.T.);
#3290=EDGE_LOOP('',(#18037,#18038,#18039,#18040));
#3291=EDGE_LOOP('',(#18041,#18042,#18043,#18044));
#3292=EDGE_LOOP('',(#18045,#18046,#18047,#18048));
#3293=EDGE_LOOP('',(#18049,#18050,#18051,#18052));
#3294=EDGE_LOOP('',(#18053,#18054,#18055,#18056));
#3295=EDGE_LOOP('',(#18057,#18058,#18059,#18060));
#3296=EDGE_LOOP('',(#18061,#18062,#18063,#18064));
#3297=EDGE_LOOP('',(#18065,#18066,#18067,#18068));
#3298=EDGE_LOOP('',(#18069,#18070,#18071,#18072));
#3299=EDGE_LOOP('',(#18073,#18074,#18075,#18076));
#3300=EDGE_LOOP('',(#18077,#18078,#18079,#18080));
#3301=EDGE_LOOP('',(#18081,#18082,#18083,#18084));
#3302=EDGE_LOOP('',(#18085,#18086,#18087,#18088));
#3303=EDGE_LOOP('',(#18089,#18090,#18091,#18092));
#3304=EDGE_LOOP('',(#18093,#18094,#18095,#18096));
#3305=EDGE_LOOP('',(#18097,#18098,#18099,#18100));
#3306=EDGE_LOOP('',(#18101,#18102,#18103,#18104,#18105,#18106,#18107,#18108,
#18109,#18110,#18111,#18112,#18113,#18114,#18115,#18116,#18117,#18118,#18119,
#18120,#18121,#18122,#18123,#18124,#18125,#18126,#18127,#18128,#18129,#18130,
#18131,#18132,#18133,#18134));
#3307=EDGE_LOOP('',(#18135,#18136,#18137,#18138));
#3308=EDGE_LOOP('',(#18139,#18140,#18141,#18142));
#3309=EDGE_LOOP('',(#18143,#18144,#18145,#18146));
#3310=EDGE_LOOP('',(#18147,#18148,#18149,#18150));
#3311=EDGE_LOOP('',(#18151,#18152,#18153,#18154));
#3312=EDGE_LOOP('',(#18155,#18156,#18157,#18158));
#3313=EDGE_LOOP('',(#18159,#18160,#18161,#18162));
#3314=EDGE_LOOP('',(#18163,#18164,#18165,#18166));
#3315=EDGE_LOOP('',(#18167,#18168,#18169,#18170));
#3316=EDGE_LOOP('',(#18171,#18172,#18173,#18174));
#3317=EDGE_LOOP('',(#18175,#18176,#18177,#18178));
#3318=EDGE_LOOP('',(#18179,#18180,#18181,#18182));
#3319=EDGE_LOOP('',(#18183,#18184,#18185,#18186));
#3320=EDGE_LOOP('',(#18187,#18188,#18189,#18190));
#3321=EDGE_LOOP('',(#18191,#18192,#18193,#18194));
#3322=EDGE_LOOP('',(#18195,#18196,#18197,#18198));
#3323=EDGE_LOOP('',(#18199,#18200,#18201,#18202));
#3324=EDGE_LOOP('',(#18203,#18204,#18205,#18206));
#3325=EDGE_LOOP('',(#18207,#18208,#18209,#18210,#18211,#18212,#18213,#18214,
#18215,#18216,#18217,#18218,#18219,#18220,#18221,#18222,#18223,#18224,#18225,
#18226,#18227,#18228,#18229,#18230,#18231,#18232,#18233,#18234,#18235,#18236,
#18237,#18238,#18239,#18240));
#3915=CIRCLE('',#21739,0.450000000000145);
#3916=CIRCLE('',#21740,0.450000000000145);
#3917=CIRCLE('',#21742,2.46743797397102);
#3918=CIRCLE('',#21743,2.46743797397102);
#3919=CIRCLE('',#21745,0.725000000000007);
#3920=CIRCLE('',#21746,0.725000000000007);
#3921=CIRCLE('',#21749,0.599999999999981);
#3922=CIRCLE('',#21750,0.599999999999981);
#3923=CIRCLE('',#21752,2.3640229247478);
#3924=CIRCLE('',#21753,2.3640229247478);
#3925=CIRCLE('',#21755,1.39999999999995);
#3926=CIRCLE('',#21756,1.39999999999995);
#3927=CIRCLE('',#21759,1.05000000000001);
#3928=CIRCLE('',#21760,1.05000000000001);
#3929=CIRCLE('',#21763,1.04999999999996);
#3930=CIRCLE('',#21764,1.04999999999996);
#3931=CIRCLE('',#21767,1.09999999999999);
#3932=CIRCLE('',#21768,1.09999999999999);
#3933=CIRCLE('',#21772,1.09999999999999);
#3934=CIRCLE('',#21773,1.04999999999996);
#3935=CIRCLE('',#21774,1.05000000000001);
#3936=CIRCLE('',#21775,1.39999999999995);
#3937=CIRCLE('',#21776,2.3640229247478);
#3938=CIRCLE('',#21777,0.599999999999981);
#3939=CIRCLE('',#21778,0.725000000000007);
#3940=CIRCLE('',#21779,2.46743797397102);
#3941=CIRCLE('',#21780,0.450000000000145);
#3942=CIRCLE('',#21783,0.450000000000145);
#3943=CIRCLE('',#21785,2.46743797397102);
#3944=CIRCLE('',#21787,0.725000000000007);
#3945=CIRCLE('',#21790,0.599999999999981);
#3946=CIRCLE('',#21792,2.3640229247478);
#3947=CIRCLE('',#21794,1.39999999999995);
#3948=CIRCLE('',#21797,1.05000000000001);
#3949=CIRCLE('',#21800,1.04999999999996);
#3950=CIRCLE('',#21803,1.09999999999999);
#5703=LINE('',#47821,#7584);
#5704=LINE('',#47823,#7585);
#5705=LINE('',#47825,#7586);
#5706=LINE('',#47826,#7587);
#5707=LINE('',#47831,#7588);
#5708=LINE('',#47837,#7589);
#5709=LINE('',#47843,#7590);
#5710=LINE('',#47847,#7591);
#5711=LINE('',#47849,#7592);
#5712=LINE('',#47850,#7593);
#5713=LINE('',#47855,#7594);
#5714=LINE('',#47861,#7595);
#5715=LINE('',#47867,#7596);
#5716=LINE('',#47871,#7597);
#5717=LINE('',#47873,#7598);
#5718=LINE('',#47874,#7599);
#5719=LINE('',#47879,#7600);
#5720=LINE('',#47883,#7601);
#5721=LINE('',#47885,#7602);
#5722=LINE('',#47886,#7603);
#5723=LINE('',#47891,#7604);
#5724=LINE('',#47895,#7605);
#5725=LINE('',#47897,#7606);
#5726=LINE('',#47898,#7607);
#5727=LINE('',#47903,#7608);
#5728=LINE('',#47907,#7609);
#5729=LINE('',#47909,#7610);
#5730=LINE('',#47910,#7611);
#5731=LINE('',#47913,#7612);
#5732=LINE('',#47915,#7613);
#5733=LINE('',#47916,#7614);
#5734=LINE('',#47919,#7615);
#5735=LINE('',#47921,#7616);
#5736=LINE('',#47923,#7617);
#5737=LINE('',#47925,#7618);
#5738=LINE('',#47929,#7619);
#5739=LINE('',#47933,#7620);
#5740=LINE('',#47937,#7621);
#5741=LINE('',#47945,#7622);
#5742=LINE('',#47952,#7623);
#5743=LINE('',#47955,#7624);
#5744=LINE('',#47957,#7625);
#5745=LINE('',#47958,#7626);
#5746=LINE('',#47961,#7627);
#5747=LINE('',#47965,#7628);
#5748=LINE('',#47969,#7629);
#5749=LINE('',#47973,#7630);
#5750=LINE('',#47974,#7631);
#5751=LINE('',#47977,#7632);
#5752=LINE('',#47981,#7633);
#5753=LINE('',#47985,#7634);
#5754=LINE('',#47989,#7635);
#5755=LINE('',#47990,#7636);
#5756=LINE('',#47993,#7637);
#5757=LINE('',#47997,#7638);
#5758=LINE('',#47998,#7639);
#5759=LINE('',#48001,#7640);
#5760=LINE('',#48005,#7641);
#5761=LINE('',#48006,#7642);
#5762=LINE('',#48009,#7643);
#5763=LINE('',#48013,#7644);
#5764=LINE('',#48014,#7645);
#5765=LINE('',#48017,#7646);
#5766=LINE('',#48018,#7647);
#5767=LINE('',#48020,#7648);
#5768=LINE('',#48022,#7649);
#7584=VECTOR('',#26600,10.);
#7585=VECTOR('',#26601,10.);
#7586=VECTOR('',#26602,10.);
#7587=VECTOR('',#26603,10.);
#7588=VECTOR('',#26608,10.);
#7589=VECTOR('',#26615,10.);
#7590=VECTOR('',#26622,10.);
#7591=VECTOR('',#26627,10.);
#7592=VECTOR('',#26628,10.);
#7593=VECTOR('',#26629,10.);
#7594=VECTOR('',#26634,10.);
#7595=VECTOR('',#26641,10.);
#7596=VECTOR('',#26648,10.);
#7597=VECTOR('',#26653,10.);
#7598=VECTOR('',#26654,10.);
#7599=VECTOR('',#26655,10.);
#7600=VECTOR('',#26660,10.);
#7601=VECTOR('',#26665,10.);
#7602=VECTOR('',#26666,10.);
#7603=VECTOR('',#26667,10.);
#7604=VECTOR('',#26672,10.);
#7605=VECTOR('',#26677,10.);
#7606=VECTOR('',#26678,10.);
#7607=VECTOR('',#26679,10.);
#7608=VECTOR('',#26684,10.);
#7609=VECTOR('',#26689,10.);
#7610=VECTOR('',#26690,10.);
#7611=VECTOR('',#26691,10.);
#7612=VECTOR('',#26694,10.);
#7613=VECTOR('',#26695,10.);
#7614=VECTOR('',#26696,10.);
#7615=VECTOR('',#26699,10.);
#7616=VECTOR('',#26700,10.);
#7617=VECTOR('',#26701,10.);
#7618=VECTOR('',#26702,10.);
#7619=VECTOR('',#26705,10.);
#7620=VECTOR('',#26708,10.);
#7621=VECTOR('',#26711,10.);
#7622=VECTOR('',#26718,10.);
#7623=VECTOR('',#26725,10.);
#7624=VECTOR('',#26728,10.);
#7625=VECTOR('',#26729,10.);
#7626=VECTOR('',#26730,10.);
#7627=VECTOR('',#26733,10.);
#7628=VECTOR('',#26738,10.);
#7629=VECTOR('',#26743,10.);
#7630=VECTOR('',#26748,10.);
#7631=VECTOR('',#26749,10.);
#7632=VECTOR('',#26752,10.);
#7633=VECTOR('',#26757,10.);
#7634=VECTOR('',#26762,10.);
#7635=VECTOR('',#26767,10.);
#7636=VECTOR('',#26768,10.);
#7637=VECTOR('',#26771,10.);
#7638=VECTOR('',#26776,10.);
#7639=VECTOR('',#26777,10.);
#7640=VECTOR('',#26780,10.);
#7641=VECTOR('',#26785,10.);
#7642=VECTOR('',#26786,10.);
#7643=VECTOR('',#26789,10.);
#7644=VECTOR('',#26794,10.);
#7645=VECTOR('',#26795,10.);
#7646=VECTOR('',#26798,10.);
#7647=VECTOR('',#26799,10.);
#7648=VECTOR('',#26802,10.);
#7649=VECTOR('',#26805,10.);
#9543=VERTEX_POINT('',#47819);
#9544=VERTEX_POINT('',#47820);
#9545=VERTEX_POINT('',#47822);
#9546=VERTEX_POINT('',#47824);
#9547=VERTEX_POINT('',#47828);
#9548=VERTEX_POINT('',#47830);
#9549=VERTEX_POINT('',#47834);
#9550=VERTEX_POINT('',#47836);
#9551=VERTEX_POINT('',#47840);
#9552=VERTEX_POINT('',#47842);
#9553=VERTEX_POINT('',#47846);
#9554=VERTEX_POINT('',#47848);
#9555=VERTEX_POINT('',#47852);
#9556=VERTEX_POINT('',#47854);
#9557=VERTEX_POINT('',#47858);
#9558=VERTEX_POINT('',#47860);
#9559=VERTEX_POINT('',#47864);
#9560=VERTEX_POINT('',#47866);
#9561=VERTEX_POINT('',#47870);
#9562=VERTEX_POINT('',#47872);
#9563=VERTEX_POINT('',#47876);
#9564=VERTEX_POINT('',#47878);
#9565=VERTEX_POINT('',#47882);
#9566=VERTEX_POINT('',#47884);
#9567=VERTEX_POINT('',#47888);
#9568=VERTEX_POINT('',#47890);
#9569=VERTEX_POINT('',#47894);
#9570=VERTEX_POINT('',#47896);
#9571=VERTEX_POINT('',#47900);
#9572=VERTEX_POINT('',#47902);
#9573=VERTEX_POINT('',#47906);
#9574=VERTEX_POINT('',#47908);
#9575=VERTEX_POINT('',#47912);
#9576=VERTEX_POINT('',#47914);
#9577=VERTEX_POINT('',#47918);
#9578=VERTEX_POINT('',#47920);
#9579=VERTEX_POINT('',#47922);
#9580=VERTEX_POINT('',#47924);
#9581=VERTEX_POINT('',#47926);
#9582=VERTEX_POINT('',#47928);
#9583=VERTEX_POINT('',#47930);
#9584=VERTEX_POINT('',#47932);
#9585=VERTEX_POINT('',#47934);
#9586=VERTEX_POINT('',#47936);
#9587=VERTEX_POINT('',#47938);
#9588=VERTEX_POINT('',#47940);
#9589=VERTEX_POINT('',#47942);
#9590=VERTEX_POINT('',#47944);
#9591=VERTEX_POINT('',#47946);
#9592=VERTEX_POINT('',#47948);
#9593=VERTEX_POINT('',#47950);
#9594=VERTEX_POINT('',#47954);
#9595=VERTEX_POINT('',#47956);
#9596=VERTEX_POINT('',#47960);
#9597=VERTEX_POINT('',#47964);
#9598=VERTEX_POINT('',#47968);
#9599=VERTEX_POINT('',#47972);
#9600=VERTEX_POINT('',#47976);
#9601=VERTEX_POINT('',#47980);
#9602=VERTEX_POINT('',#47984);
#9603=VERTEX_POINT('',#47988);
#9604=VERTEX_POINT('',#47992);
#9605=VERTEX_POINT('',#47996);
#9606=VERTEX_POINT('',#48000);
#9607=VERTEX_POINT('',#48004);
#9608=VERTEX_POINT('',#48008);
#9609=VERTEX_POINT('',#48012);
#9610=VERTEX_POINT('',#48016);
#12402=EDGE_CURVE('',#9543,#9544,#5703,.T.);
#12403=EDGE_CURVE('',#9545,#9543,#5704,.T.);
#12404=EDGE_CURVE('',#9546,#9545,#5705,.T.);
#12405=EDGE_CURVE('',#9544,#9546,#5706,.T.);
#12406=EDGE_CURVE('',#9547,#9545,#3915,.T.);
#12407=EDGE_CURVE('',#9548,#9547,#5707,.T.);
#12408=EDGE_CURVE('',#9546,#9548,#3916,.T.);
#12409=EDGE_CURVE('',#9549,#9547,#3917,.T.);
#12410=EDGE_CURVE('',#9550,#9549,#5708,.T.);
#12411=EDGE_CURVE('',#9548,#9550,#3918,.T.);
#12412=EDGE_CURVE('',#9551,#9549,#3919,.T.);
#12413=EDGE_CURVE('',#9552,#9551,#5709,.T.);
#12414=EDGE_CURVE('',#9550,#9552,#3920,.T.);
#12415=EDGE_CURVE('',#9553,#9551,#5710,.T.);
#12416=EDGE_CURVE('',#9554,#9553,#5711,.T.);
#12417=EDGE_CURVE('',#9552,#9554,#5712,.T.);
#12418=EDGE_CURVE('',#9555,#9553,#3921,.T.);
#12419=EDGE_CURVE('',#9556,#9555,#5713,.T.);
#12420=EDGE_CURVE('',#9554,#9556,#3922,.T.);
#12421=EDGE_CURVE('',#9557,#9555,#3923,.T.);
#12422=EDGE_CURVE('',#9558,#9557,#5714,.T.);
#12423=EDGE_CURVE('',#9556,#9558,#3924,.T.);
#12424=EDGE_CURVE('',#9559,#9557,#3925,.T.);
#12425=EDGE_CURVE('',#9560,#9559,#5715,.T.);
#12426=EDGE_CURVE('',#9558,#9560,#3926,.T.);
#12427=EDGE_CURVE('',#9561,#9559,#5716,.T.);
#12428=EDGE_CURVE('',#9562,#9561,#5717,.T.);
#12429=EDGE_CURVE('',#9560,#9562,#5718,.T.);
#12430=EDGE_CURVE('',#9563,#9561,#3927,.T.);
#12431=EDGE_CURVE('',#9564,#9563,#5719,.T.);
#12432=EDGE_CURVE('',#9562,#9564,#3928,.T.);
#12433=EDGE_CURVE('',#9565,#9563,#5720,.T.);
#12434=EDGE_CURVE('',#9566,#9565,#5721,.T.);
#12435=EDGE_CURVE('',#9564,#9566,#5722,.T.);
#12436=EDGE_CURVE('',#9567,#9565,#3929,.T.);
#12437=EDGE_CURVE('',#9568,#9567,#5723,.T.);
#12438=EDGE_CURVE('',#9566,#9568,#3930,.T.);
#12439=EDGE_CURVE('',#9569,#9567,#5724,.T.);
#12440=EDGE_CURVE('',#9570,#9569,#5725,.T.);
#12441=EDGE_CURVE('',#9568,#9570,#5726,.T.);
#12442=EDGE_CURVE('',#9571,#9569,#3931,.T.);
#12443=EDGE_CURVE('',#9572,#9571,#5727,.T.);
#12444=EDGE_CURVE('',#9570,#9572,#3932,.T.);
#12445=EDGE_CURVE('',#9573,#9571,#5728,.T.);
#12446=EDGE_CURVE('',#9574,#9573,#5729,.T.);
#12447=EDGE_CURVE('',#9572,#9574,#5730,.T.);
#12448=EDGE_CURVE('',#9575,#9573,#5731,.T.);
#12449=EDGE_CURVE('',#9576,#9575,#5732,.T.);
#12450=EDGE_CURVE('',#9574,#9576,#5733,.T.);
#12451=EDGE_CURVE('',#9577,#9544,#5734,.T.);
#12452=EDGE_CURVE('',#9578,#9576,#5735,.T.);
#12453=EDGE_CURVE('',#9579,#9578,#5736,.T.);
#12454=EDGE_CURVE('',#9580,#9579,#5737,.T.);
#12455=EDGE_CURVE('',#9581,#9580,#3933,.T.);
#12456=EDGE_CURVE('',#9582,#9581,#5738,.T.);
#12457=EDGE_CURVE('',#9583,#9582,#3934,.T.);
#12458=EDGE_CURVE('',#9584,#9583,#5739,.T.);
#12459=EDGE_CURVE('',#9585,#9584,#3935,.T.);
#12460=EDGE_CURVE('',#9586,#9585,#5740,.T.);
#12461=EDGE_CURVE('',#9587,#9586,#3936,.T.);
#12462=EDGE_CURVE('',#9588,#9587,#3937,.T.);
#12463=EDGE_CURVE('',#9589,#9588,#3938,.T.);
#12464=EDGE_CURVE('',#9590,#9589,#5741,.T.);
#12465=EDGE_CURVE('',#9591,#9590,#3939,.T.);
#12466=EDGE_CURVE('',#9592,#9591,#3940,.T.);
#12467=EDGE_CURVE('',#9593,#9592,#3941,.T.);
#12468=EDGE_CURVE('',#9577,#9593,#5742,.T.);
#12469=EDGE_CURVE('',#9594,#9577,#5743,.T.);
#12470=EDGE_CURVE('',#9593,#9595,#5744,.T.);
#12471=EDGE_CURVE('',#9595,#9594,#5745,.T.);
#12472=EDGE_CURVE('',#9592,#9596,#5746,.T.);
#12473=EDGE_CURVE('',#9596,#9595,#3942,.T.);
#12474=EDGE_CURVE('',#9591,#9597,#5747,.T.);
#12475=EDGE_CURVE('',#9597,#9596,#3943,.T.);
#12476=EDGE_CURVE('',#9590,#9598,#5748,.T.);
#12477=EDGE_CURVE('',#9598,#9597,#3944,.T.);
#12478=EDGE_CURVE('',#9589,#9599,#5749,.T.);
#12479=EDGE_CURVE('',#9599,#9598,#5750,.T.);
#12480=EDGE_CURVE('',#9588,#9600,#5751,.T.);
#12481=EDGE_CURVE('',#9600,#9599,#3945,.T.);
#12482=EDGE_CURVE('',#9587,#9601,#5752,.T.);
#12483=EDGE_CURVE('',#9601,#9600,#3946,.T.);
#12484=EDGE_CURVE('',#9586,#9602,#5753,.T.);
#12485=EDGE_CURVE('',#9602,#9601,#3947,.T.);
#12486=EDGE_CURVE('',#9585,#9603,#5754,.T.);
#12487=EDGE_CURVE('',#9603,#9602,#5755,.T.);
#12488=EDGE_CURVE('',#9584,#9604,#5756,.T.);
#12489=EDGE_CURVE('',#9604,#9603,#3948,.T.);
#12490=EDGE_CURVE('',#9583,#9605,#5757,.T.);
#12491=EDGE_CURVE('',#9605,#9604,#5758,.T.);
#12492=EDGE_CURVE('',#9582,#9606,#5759,.T.);
#12493=EDGE_CURVE('',#9606,#9605,#3949,.T.);
#12494=EDGE_CURVE('',#9581,#9607,#5760,.T.);
#12495=EDGE_CURVE('',#9607,#9606,#5761,.T.);
#12496=EDGE_CURVE('',#9580,#9608,#5762,.T.);
#12497=EDGE_CURVE('',#9608,#9607,#3950,.T.);
#12498=EDGE_CURVE('',#9579,#9609,#5763,.T.);
#12499=EDGE_CURVE('',#9609,#9608,#5764,.T.);
#12500=EDGE_CURVE('',#9578,#9610,#5765,.T.);
#12501=EDGE_CURVE('',#9610,#9609,#5766,.T.);
#12502=EDGE_CURVE('',#9610,#9575,#5767,.T.);
#12503=EDGE_CURVE('',#9594,#9543,#5768,.T.);
#18037=ORIENTED_EDGE('',*,*,#12402,.F.);
#18038=ORIENTED_EDGE('',*,*,#12403,.F.);
#18039=ORIENTED_EDGE('',*,*,#12404,.F.);
#18040=ORIENTED_EDGE('',*,*,#12405,.F.);
#18041=ORIENTED_EDGE('',*,*,#12404,.T.);
#18042=ORIENTED_EDGE('',*,*,#12406,.F.);
#18043=ORIENTED_EDGE('',*,*,#12407,.F.);
#18044=ORIENTED_EDGE('',*,*,#12408,.F.);
#18045=ORIENTED_EDGE('',*,*,#12407,.T.);
#18046=ORIENTED_EDGE('',*,*,#12409,.F.);
#18047=ORIENTED_EDGE('',*,*,#12410,.F.);
#18048=ORIENTED_EDGE('',*,*,#12411,.F.);
#18049=ORIENTED_EDGE('',*,*,#12410,.T.);
#18050=ORIENTED_EDGE('',*,*,#12412,.F.);
#18051=ORIENTED_EDGE('',*,*,#12413,.F.);
#18052=ORIENTED_EDGE('',*,*,#12414,.F.);
#18053=ORIENTED_EDGE('',*,*,#12413,.T.);
#18054=ORIENTED_EDGE('',*,*,#12415,.F.);
#18055=ORIENTED_EDGE('',*,*,#12416,.F.);
#18056=ORIENTED_EDGE('',*,*,#12417,.F.);
#18057=ORIENTED_EDGE('',*,*,#12416,.T.);
#18058=ORIENTED_EDGE('',*,*,#12418,.F.);
#18059=ORIENTED_EDGE('',*,*,#12419,.F.);
#18060=ORIENTED_EDGE('',*,*,#12420,.F.);
#18061=ORIENTED_EDGE('',*,*,#12419,.T.);
#18062=ORIENTED_EDGE('',*,*,#12421,.F.);
#18063=ORIENTED_EDGE('',*,*,#12422,.F.);
#18064=ORIENTED_EDGE('',*,*,#12423,.F.);
#18065=ORIENTED_EDGE('',*,*,#12422,.T.);
#18066=ORIENTED_EDGE('',*,*,#12424,.F.);
#18067=ORIENTED_EDGE('',*,*,#12425,.F.);
#18068=ORIENTED_EDGE('',*,*,#12426,.F.);
#18069=ORIENTED_EDGE('',*,*,#12425,.T.);
#18070=ORIENTED_EDGE('',*,*,#12427,.F.);
#18071=ORIENTED_EDGE('',*,*,#12428,.F.);
#18072=ORIENTED_EDGE('',*,*,#12429,.F.);
#18073=ORIENTED_EDGE('',*,*,#12428,.T.);
#18074=ORIENTED_EDGE('',*,*,#12430,.F.);
#18075=ORIENTED_EDGE('',*,*,#12431,.F.);
#18076=ORIENTED_EDGE('',*,*,#12432,.F.);
#18077=ORIENTED_EDGE('',*,*,#12431,.T.);
#18078=ORIENTED_EDGE('',*,*,#12433,.F.);
#18079=ORIENTED_EDGE('',*,*,#12434,.F.);
#18080=ORIENTED_EDGE('',*,*,#12435,.F.);
#18081=ORIENTED_EDGE('',*,*,#12434,.T.);
#18082=ORIENTED_EDGE('',*,*,#12436,.F.);
#18083=ORIENTED_EDGE('',*,*,#12437,.F.);
#18084=ORIENTED_EDGE('',*,*,#12438,.F.);
#18085=ORIENTED_EDGE('',*,*,#12437,.T.);
#18086=ORIENTED_EDGE('',*,*,#12439,.F.);
#18087=ORIENTED_EDGE('',*,*,#12440,.F.);
#18088=ORIENTED_EDGE('',*,*,#12441,.F.);
#18089=ORIENTED_EDGE('',*,*,#12440,.T.);
#18090=ORIENTED_EDGE('',*,*,#12442,.F.);
#18091=ORIENTED_EDGE('',*,*,#12443,.F.);
#18092=ORIENTED_EDGE('',*,*,#12444,.F.);
#18093=ORIENTED_EDGE('',*,*,#12443,.T.);
#18094=ORIENTED_EDGE('',*,*,#12445,.F.);
#18095=ORIENTED_EDGE('',*,*,#12446,.F.);
#18096=ORIENTED_EDGE('',*,*,#12447,.F.);
#18097=ORIENTED_EDGE('',*,*,#12446,.T.);
#18098=ORIENTED_EDGE('',*,*,#12448,.F.);
#18099=ORIENTED_EDGE('',*,*,#12449,.F.);
#18100=ORIENTED_EDGE('',*,*,#12450,.F.);
#18101=ORIENTED_EDGE('',*,*,#12451,.T.);
#18102=ORIENTED_EDGE('',*,*,#12405,.T.);
#18103=ORIENTED_EDGE('',*,*,#12408,.T.);
#18104=ORIENTED_EDGE('',*,*,#12411,.T.);
#18105=ORIENTED_EDGE('',*,*,#12414,.T.);
#18106=ORIENTED_EDGE('',*,*,#12417,.T.);
#18107=ORIENTED_EDGE('',*,*,#12420,.T.);
#18108=ORIENTED_EDGE('',*,*,#12423,.T.);
#18109=ORIENTED_EDGE('',*,*,#12426,.T.);
#18110=ORIENTED_EDGE('',*,*,#12429,.T.);
#18111=ORIENTED_EDGE('',*,*,#12432,.T.);
#18112=ORIENTED_EDGE('',*,*,#12435,.T.);
#18113=ORIENTED_EDGE('',*,*,#12438,.T.);
#18114=ORIENTED_EDGE('',*,*,#12441,.T.);
#18115=ORIENTED_EDGE('',*,*,#12444,.T.);
#18116=ORIENTED_EDGE('',*,*,#12447,.T.);
#18117=ORIENTED_EDGE('',*,*,#12450,.T.);
#18118=ORIENTED_EDGE('',*,*,#12452,.F.);
#18119=ORIENTED_EDGE('',*,*,#12453,.F.);
#18120=ORIENTED_EDGE('',*,*,#12454,.F.);
#18121=ORIENTED_EDGE('',*,*,#12455,.F.);
#18122=ORIENTED_EDGE('',*,*,#12456,.F.);
#18123=ORIENTED_EDGE('',*,*,#12457,.F.);
#18124=ORIENTED_EDGE('',*,*,#12458,.F.);
#18125=ORIENTED_EDGE('',*,*,#12459,.F.);
#18126=ORIENTED_EDGE('',*,*,#12460,.F.);
#18127=ORIENTED_EDGE('',*,*,#12461,.F.);
#18128=ORIENTED_EDGE('',*,*,#12462,.F.);
#18129=ORIENTED_EDGE('',*,*,#12463,.F.);
#18130=ORIENTED_EDGE('',*,*,#12464,.F.);
#18131=ORIENTED_EDGE('',*,*,#12465,.F.);
#18132=ORIENTED_EDGE('',*,*,#12466,.F.);
#18133=ORIENTED_EDGE('',*,*,#12467,.F.);
#18134=ORIENTED_EDGE('',*,*,#12468,.F.);
#18135=ORIENTED_EDGE('',*,*,#12469,.T.);
#18136=ORIENTED_EDGE('',*,*,#12468,.T.);
#18137=ORIENTED_EDGE('',*,*,#12470,.T.);
#18138=ORIENTED_EDGE('',*,*,#12471,.T.);
#18139=ORIENTED_EDGE('',*,*,#12470,.F.);
#18140=ORIENTED_EDGE('',*,*,#12467,.T.);
#18141=ORIENTED_EDGE('',*,*,#12472,.T.);
#18142=ORIENTED_EDGE('',*,*,#12473,.T.);
#18143=ORIENTED_EDGE('',*,*,#12472,.F.);
#18144=ORIENTED_EDGE('',*,*,#12466,.T.);
#18145=ORIENTED_EDGE('',*,*,#12474,.T.);
#18146=ORIENTED_EDGE('',*,*,#12475,.T.);
#18147=ORIENTED_EDGE('',*,*,#12474,.F.);
#18148=ORIENTED_EDGE('',*,*,#12465,.T.);
#18149=ORIENTED_EDGE('',*,*,#12476,.T.);
#18150=ORIENTED_EDGE('',*,*,#12477,.T.);
#18151=ORIENTED_EDGE('',*,*,#12476,.F.);
#18152=ORIENTED_EDGE('',*,*,#12464,.T.);
#18153=ORIENTED_EDGE('',*,*,#12478,.T.);
#18154=ORIENTED_EDGE('',*,*,#12479,.T.);
#18155=ORIENTED_EDGE('',*,*,#12478,.F.);
#18156=ORIENTED_EDGE('',*,*,#12463,.T.);
#18157=ORIENTED_EDGE('',*,*,#12480,.T.);
#18158=ORIENTED_EDGE('',*,*,#12481,.T.);
#18159=ORIENTED_EDGE('',*,*,#12480,.F.);
#18160=ORIENTED_EDGE('',*,*,#12462,.T.);
#18161=ORIENTED_EDGE('',*,*,#12482,.T.);
#18162=ORIENTED_EDGE('',*,*,#12483,.T.);
#18163=ORIENTED_EDGE('',*,*,#12482,.F.);
#18164=ORIENTED_EDGE('',*,*,#12461,.T.);
#18165=ORIENTED_EDGE('',*,*,#12484,.T.);
#18166=ORIENTED_EDGE('',*,*,#12485,.T.);
#18167=ORIENTED_EDGE('',*,*,#12484,.F.);
#18168=ORIENTED_EDGE('',*,*,#12460,.T.);
#18169=ORIENTED_EDGE('',*,*,#12486,.T.);
#18170=ORIENTED_EDGE('',*,*,#12487,.T.);
#18171=ORIENTED_EDGE('',*,*,#12486,.F.);
#18172=ORIENTED_EDGE('',*,*,#12459,.T.);
#18173=ORIENTED_EDGE('',*,*,#12488,.T.);
#18174=ORIENTED_EDGE('',*,*,#12489,.T.);
#18175=ORIENTED_EDGE('',*,*,#12488,.F.);
#18176=ORIENTED_EDGE('',*,*,#12458,.T.);
#18177=ORIENTED_EDGE('',*,*,#12490,.T.);
#18178=ORIENTED_EDGE('',*,*,#12491,.T.);
#18179=ORIENTED_EDGE('',*,*,#12490,.F.);
#18180=ORIENTED_EDGE('',*,*,#12457,.T.);
#18181=ORIENTED_EDGE('',*,*,#12492,.T.);
#18182=ORIENTED_EDGE('',*,*,#12493,.T.);
#18183=ORIENTED_EDGE('',*,*,#12492,.F.);
#18184=ORIENTED_EDGE('',*,*,#12456,.T.);
#18185=ORIENTED_EDGE('',*,*,#12494,.T.);
#18186=ORIENTED_EDGE('',*,*,#12495,.T.);
#18187=ORIENTED_EDGE('',*,*,#12494,.F.);
#18188=ORIENTED_EDGE('',*,*,#12455,.T.);
#18189=ORIENTED_EDGE('',*,*,#12496,.T.);
#18190=ORIENTED_EDGE('',*,*,#12497,.T.);
#18191=ORIENTED_EDGE('',*,*,#12496,.F.);
#18192=ORIENTED_EDGE('',*,*,#12454,.T.);
#18193=ORIENTED_EDGE('',*,*,#12498,.T.);
#18194=ORIENTED_EDGE('',*,*,#12499,.T.);
#18195=ORIENTED_EDGE('',*,*,#12498,.F.);
#18196=ORIENTED_EDGE('',*,*,#12453,.T.);
#18197=ORIENTED_EDGE('',*,*,#12500,.T.);
#18198=ORIENTED_EDGE('',*,*,#12501,.T.);
#18199=ORIENTED_EDGE('',*,*,#12500,.F.);
#18200=ORIENTED_EDGE('',*,*,#12452,.T.);
#18201=ORIENTED_EDGE('',*,*,#12449,.T.);
#18202=ORIENTED_EDGE('',*,*,#12502,.F.);
#18203=ORIENTED_EDGE('',*,*,#12503,.T.);
#18204=ORIENTED_EDGE('',*,*,#12402,.T.);
#18205=ORIENTED_EDGE('',*,*,#12451,.F.);
#18206=ORIENTED_EDGE('',*,*,#12469,.F.);
#18207=ORIENTED_EDGE('',*,*,#12503,.F.);
#18208=ORIENTED_EDGE('',*,*,#12471,.F.);
#18209=ORIENTED_EDGE('',*,*,#12473,.F.);
#18210=ORIENTED_EDGE('',*,*,#12475,.F.);
#18211=ORIENTED_EDGE('',*,*,#12477,.F.);
#18212=ORIENTED_EDGE('',*,*,#12479,.F.);
#18213=ORIENTED_EDGE('',*,*,#12481,.F.);
#18214=ORIENTED_EDGE('',*,*,#12483,.F.);
#18215=ORIENTED_EDGE('',*,*,#12485,.F.);
#18216=ORIENTED_EDGE('',*,*,#12487,.F.);
#18217=ORIENTED_EDGE('',*,*,#12489,.F.);
#18218=ORIENTED_EDGE('',*,*,#12491,.F.);
#18219=ORIENTED_EDGE('',*,*,#12493,.F.);
#18220=ORIENTED_EDGE('',*,*,#12495,.F.);
#18221=ORIENTED_EDGE('',*,*,#12497,.F.);
#18222=ORIENTED_EDGE('',*,*,#12499,.F.);
#18223=ORIENTED_EDGE('',*,*,#12501,.F.);
#18224=ORIENTED_EDGE('',*,*,#12502,.T.);
#18225=ORIENTED_EDGE('',*,*,#12448,.T.);
#18226=ORIENTED_EDGE('',*,*,#12445,.T.);
#18227=ORIENTED_EDGE('',*,*,#12442,.T.);
#18228=ORIENTED_EDGE('',*,*,#12439,.T.);
#18229=ORIENTED_EDGE('',*,*,#12436,.T.);
#18230=ORIENTED_EDGE('',*,*,#12433,.T.);
#18231=ORIENTED_EDGE('',*,*,#12430,.T.);
#18232=ORIENTED_EDGE('',*,*,#12427,.T.);
#18233=ORIENTED_EDGE('',*,*,#12424,.T.);
#18234=ORIENTED_EDGE('',*,*,#12421,.T.);
#18235=ORIENTED_EDGE('',*,*,#12418,.T.);
#18236=ORIENTED_EDGE('',*,*,#12415,.T.);
#18237=ORIENTED_EDGE('',*,*,#12412,.T.);
#18238=ORIENTED_EDGE('',*,*,#12409,.T.);
#18239=ORIENTED_EDGE('',*,*,#12406,.T.);
#18240=ORIENTED_EDGE('',*,*,#12403,.T.);
#19010=PLANE('',#21737);
#19011=PLANE('',#21747);
#19012=PLANE('',#21757);
#19013=PLANE('',#21761);
#19014=PLANE('',#21765);
#19015=PLANE('',#21769);
#19016=PLANE('',#21770);
#19017=PLANE('',#21771);
#19018=PLANE('',#21781);
#19019=PLANE('',#21788);
#19020=PLANE('',#21795);
#19021=PLANE('',#21798);
#19022=PLANE('',#21801);
#19023=PLANE('',#21804);
#19024=PLANE('',#21805);
#19025=PLANE('',#21806);
#19026=PLANE('',#21807);
#19027=PLANE('',#21808);
#20015=ADVANCED_FACE('',(#2158),#19010,.T.);
#20016=ADVANCED_FACE('',(#2159),#1168,.T.);
#20017=ADVANCED_FACE('',(#2160),#1169,.F.);
#20018=ADVANCED_FACE('',(#2161),#1170,.T.);
#20019=ADVANCED_FACE('',(#2162),#19011,.T.);
#20020=ADVANCED_FACE('',(#2163),#1171,.T.);
#20021=ADVANCED_FACE('',(#2164),#1172,.F.);
#20022=ADVANCED_FACE('',(#2165),#1173,.T.);
#20023=ADVANCED_FACE('',(#2166),#19012,.T.);
#20024=ADVANCED_FACE('',(#2167),#1174,.F.);
#20025=ADVANCED_FACE('',(#2168),#19013,.T.);
#20026=ADVANCED_FACE('',(#2169),#1175,.F.);
#20027=ADVANCED_FACE('',(#2170),#19014,.T.);
#20028=ADVANCED_FACE('',(#2171),#1176,.T.);
#20029=ADVANCED_FACE('',(#2172),#19015,.T.);
#20030=ADVANCED_FACE('',(#2173),#19016,.T.);
#20031=ADVANCED_FACE('',(#2174),#19017,.T.);
#20032=ADVANCED_FACE('',(#2175),#19018,.F.);
#20033=ADVANCED_FACE('',(#2176),#1177,.T.);
#20034=ADVANCED_FACE('',(#2177),#1178,.F.);
#20035=ADVANCED_FACE('',(#2178),#1179,.T.);
#20036=ADVANCED_FACE('',(#2179),#19019,.F.);
#20037=ADVANCED_FACE('',(#2180),#1180,.T.);
#20038=ADVANCED_FACE('',(#2181),#1181,.F.);
#20039=ADVANCED_FACE('',(#2182),#1182,.T.);
#20040=ADVANCED_FACE('',(#2183),#19020,.F.);
#20041=ADVANCED_FACE('',(#2184),#1183,.F.);
#20042=ADVANCED_FACE('',(#2185),#19021,.F.);
#20043=ADVANCED_FACE('',(#2186),#1184,.F.);
#20044=ADVANCED_FACE('',(#2187),#19022,.F.);
#20045=ADVANCED_FACE('',(#2188),#1185,.T.);
#20046=ADVANCED_FACE('',(#2189),#19023,.F.);
#20047=ADVANCED_FACE('',(#2190),#19024,.F.);
#20048=ADVANCED_FACE('',(#2191),#19025,.F.);
#20049=ADVANCED_FACE('',(#2192),#19026,.F.);
#20050=ADVANCED_FACE('',(#2193),#19027,.F.);
#20129=CLOSED_SHELL('',(#20015,#20016,#20017,#20018,#20019,#20020,#20021,
#20022,#20023,#20024,#20025,#20026,#20027,#20028,#20029,#20030,#20031,#20032,
#20033,#20034,#20035,#20036,#20037,#20038,#20039,#20040,#20041,#20042,#20043,
#20044,#20045,#20046,#20047,#20048,#20049,#20050));
#21736=AXIS2_PLACEMENT_3D('',#47817,#26596,#26597);
#21737=AXIS2_PLACEMENT_3D('',#47818,#26598,#26599);
#21738=AXIS2_PLACEMENT_3D('',#47827,#26604,#26605);
#21739=AXIS2_PLACEMENT_3D('',#47829,#26606,#26607);
#21740=AXIS2_PLACEMENT_3D('',#47832,#26609,#26610);
#21741=AXIS2_PLACEMENT_3D('',#47833,#26611,#26612);
#21742=AXIS2_PLACEMENT_3D('',#47835,#26613,#26614);
#21743=AXIS2_PLACEMENT_3D('',#47838,#26616,#26617);
#21744=AXIS2_PLACEMENT_3D('',#47839,#26618,#26619);
#21745=AXIS2_PLACEMENT_3D('',#47841,#26620,#26621);
#21746=AXIS2_PLACEMENT_3D('',#47844,#26623,#26624);
#21747=AXIS2_PLACEMENT_3D('',#47845,#26625,#26626);
#21748=AXIS2_PLACEMENT_3D('',#47851,#26630,#26631);
#21749=AXIS2_PLACEMENT_3D('',#47853,#26632,#26633);
#21750=AXIS2_PLACEMENT_3D('',#47856,#26635,#26636);
#21751=AXIS2_PLACEMENT_3D('',#47857,#26637,#26638);
#21752=AXIS2_PLACEMENT_3D('',#47859,#26639,#26640);
#21753=AXIS2_PLACEMENT_3D('',#47862,#26642,#26643);
#21754=AXIS2_PLACEMENT_3D('',#47863,#26644,#26645);
#21755=AXIS2_PLACEMENT_3D('',#47865,#26646,#26647);
#21756=AXIS2_PLACEMENT_3D('',#47868,#26649,#26650);
#21757=AXIS2_PLACEMENT_3D('',#47869,#26651,#26652);
#21758=AXIS2_PLACEMENT_3D('',#47875,#26656,#26657);
#21759=AXIS2_PLACEMENT_3D('',#47877,#26658,#26659);
#21760=AXIS2_PLACEMENT_3D('',#47880,#26661,#26662);
#21761=AXIS2_PLACEMENT_3D('',#47881,#26663,#26664);
#21762=AXIS2_PLACEMENT_3D('',#47887,#26668,#26669);
#21763=AXIS2_PLACEMENT_3D('',#47889,#26670,#26671);
#21764=AXIS2_PLACEMENT_3D('',#47892,#26673,#26674);
#21765=AXIS2_PLACEMENT_3D('',#47893,#26675,#26676);
#21766=AXIS2_PLACEMENT_3D('',#47899,#26680,#26681);
#21767=AXIS2_PLACEMENT_3D('',#47901,#26682,#26683);
#21768=AXIS2_PLACEMENT_3D('',#47904,#26685,#26686);
#21769=AXIS2_PLACEMENT_3D('',#47905,#26687,#26688);
#21770=AXIS2_PLACEMENT_3D('',#47911,#26692,#26693);
#21771=AXIS2_PLACEMENT_3D('',#47917,#26697,#26698);
#21772=AXIS2_PLACEMENT_3D('',#47927,#26703,#26704);
#21773=AXIS2_PLACEMENT_3D('',#47931,#26706,#26707);
#21774=AXIS2_PLACEMENT_3D('',#47935,#26709,#26710);
#21775=AXIS2_PLACEMENT_3D('',#47939,#26712,#26713);
#21776=AXIS2_PLACEMENT_3D('',#47941,#26714,#26715);
#21777=AXIS2_PLACEMENT_3D('',#47943,#26716,#26717);
#21778=AXIS2_PLACEMENT_3D('',#47947,#26719,#26720);
#21779=AXIS2_PLACEMENT_3D('',#47949,#26721,#26722);
#21780=AXIS2_PLACEMENT_3D('',#47951,#26723,#26724);
#21781=AXIS2_PLACEMENT_3D('',#47953,#26726,#26727);
#21782=AXIS2_PLACEMENT_3D('',#47959,#26731,#26732);
#21783=AXIS2_PLACEMENT_3D('',#47962,#26734,#26735);
#21784=AXIS2_PLACEMENT_3D('',#47963,#26736,#26737);
#21785=AXIS2_PLACEMENT_3D('',#47966,#26739,#26740);
#21786=AXIS2_PLACEMENT_3D('',#47967,#26741,#26742);
#21787=AXIS2_PLACEMENT_3D('',#47970,#26744,#26745);
#21788=AXIS2_PLACEMENT_3D('',#47971,#26746,#26747);
#21789=AXIS2_PLACEMENT_3D('',#47975,#26750,#26751);
#21790=AXIS2_PLACEMENT_3D('',#47978,#26753,#26754);
#21791=AXIS2_PLACEMENT_3D('',#47979,#26755,#26756);
#21792=AXIS2_PLACEMENT_3D('',#47982,#26758,#26759);
#21793=AXIS2_PLACEMENT_3D('',#47983,#26760,#26761);
#21794=AXIS2_PLACEMENT_3D('',#47986,#26763,#26764);
#21795=AXIS2_PLACEMENT_3D('',#47987,#26765,#26766);
#21796=AXIS2_PLACEMENT_3D('',#47991,#26769,#26770);
#21797=AXIS2_PLACEMENT_3D('',#47994,#26772,#26773);
#21798=AXIS2_PLACEMENT_3D('',#47995,#26774,#26775);
#21799=AXIS2_PLACEMENT_3D('',#47999,#26778,#26779);
#21800=AXIS2_PLACEMENT_3D('',#48002,#26781,#26782);
#21801=AXIS2_PLACEMENT_3D('',#48003,#26783,#26784);
#21802=AXIS2_PLACEMENT_3D('',#48007,#26787,#26788);
#21803=AXIS2_PLACEMENT_3D('',#48010,#26790,#26791);
#21804=AXIS2_PLACEMENT_3D('',#48011,#26792,#26793);
#21805=AXIS2_PLACEMENT_3D('',#48015,#26796,#26797);
#21806=AXIS2_PLACEMENT_3D('',#48019,#26800,#26801);
#21807=AXIS2_PLACEMENT_3D('',#48021,#26803,#26804);
#21808=AXIS2_PLACEMENT_3D('',#48023,#26806,#26807);
#26596=DIRECTION('axis',(0.,0.,1.));
#26597=DIRECTION('refdir',(1.,0.,0.));
#26598=DIRECTION('center_axis',(0.710729249896214,0.,0.703465658964221));
#26599=DIRECTION('ref_axis',(-0.703465658964221,0.,0.710729249896214));
#26600=DIRECTION('',(0.,1.,0.));
#26601=DIRECTION('',(-0.703465658964221,0.,0.710729249896214));
#26602=DIRECTION('',(0.,-1.,0.));
#26603=DIRECTION('',(0.703465658964221,0.,-0.710729249896214));
#26604=DIRECTION('center_axis',(0.,-1.,0.));
#26605=DIRECTION('ref_axis',(0.963381374692954,0.,0.268134904282738));
#26606=DIRECTION('center_axis',(0.,-1.,0.));
#26607=DIRECTION('ref_axis',(0.963381374692954,0.,0.268134904282738));
#26608=DIRECTION('',(0.,-1.,0.));
#26609=DIRECTION('center_axis',(0.,1.,0.));
#26610=DIRECTION('ref_axis',(0.963381374692954,0.,0.268134904282738));
#26611=DIRECTION('center_axis',(0.,-1.,0.));
#26612=DIRECTION('ref_axis',(-0.963381374692978,0.,-0.268134904282653));
#26613=DIRECTION('center_axis',(0.,1.,0.));
#26614=DIRECTION('ref_axis',(-0.963381374692978,0.,-0.268134904282653));
#26615=DIRECTION('',(0.,-1.,0.));
#26616=DIRECTION('center_axis',(0.,-1.,0.));
#26617=DIRECTION('ref_axis',(-0.963381374692978,0.,-0.268134904282653));
#26618=DIRECTION('center_axis',(0.,-1.,0.));
#26619=DIRECTION('ref_axis',(1.,0.,-2.53764096072769E-16));
#26620=DIRECTION('center_axis',(0.,-1.,0.));
#26621=DIRECTION('ref_axis',(1.,0.,-2.53764096072769E-16));
#26622=DIRECTION('',(0.,-1.,0.));
#26623=DIRECTION('center_axis',(0.,1.,0.));
#26624=DIRECTION('ref_axis',(1.,0.,-2.53764096072769E-16));
#26625=DIRECTION('center_axis',(1.,0.,-2.53764096072769E-16));
#26626=DIRECTION('ref_axis',(2.53764096072769E-16,0.,1.));
#26627=DIRECTION('',(2.53764096072769E-16,0.,1.));
#26628=DIRECTION('',(0.,-1.,0.));
#26629=DIRECTION('',(-2.53764096072769E-16,0.,-1.));
#26630=DIRECTION('center_axis',(0.,-1.,0.));
#26631=DIRECTION('ref_axis',(0.245760053518537,0.,-0.969330694909929));
#26632=DIRECTION('center_axis',(0.,-1.,0.));
#26633=DIRECTION('ref_axis',(0.245760053518537,0.,-0.969330694909929));
#26634=DIRECTION('',(0.,-1.,0.));
#26635=DIRECTION('center_axis',(0.,1.,0.));
#26636=DIRECTION('ref_axis',(0.245760053518537,0.,-0.969330694909929));
#26637=DIRECTION('center_axis',(0.,-1.,0.));
#26638=DIRECTION('ref_axis',(-0.245760053518569,0.,0.969330694909921));
#26639=DIRECTION('center_axis',(0.,1.,0.));
#26640=DIRECTION('ref_axis',(-0.245760053518569,0.,0.969330694909921));
#26641=DIRECTION('',(0.,-1.,0.));
#26642=DIRECTION('center_axis',(0.,-1.,0.));
#26643=DIRECTION('ref_axis',(-0.245760053518569,0.,0.969330694909921));
#26644=DIRECTION('center_axis',(0.,-1.,0.));
#26645=DIRECTION('ref_axis',(0.711979844231348,0.,-0.702199901316075));
#26646=DIRECTION('center_axis',(0.,-1.,0.));
#26647=DIRECTION('ref_axis',(0.711979844231348,0.,-0.702199901316075));
#26648=DIRECTION('',(0.,-1.,0.));
#26649=DIRECTION('center_axis',(0.,1.,0.));
#26650=DIRECTION('ref_axis',(0.711979844231348,0.,-0.702199901316075));
#26651=DIRECTION('center_axis',(0.71197984423134,0.,-0.702199901316083));
#26652=DIRECTION('ref_axis',(0.702199901316083,0.,0.71197984423134));
#26653=DIRECTION('',(0.702199901316083,0.,0.71197984423134));
#26654=DIRECTION('',(0.,-1.,0.));
#26655=DIRECTION('',(-0.702199901316083,0.,-0.71197984423134));
#26656=DIRECTION('center_axis',(0.,-1.,0.));
#26657=DIRECTION('ref_axis',(-0.711979844231334,0.,0.702199901316089));
#26658=DIRECTION('center_axis',(0.,1.,0.));
#26659=DIRECTION('ref_axis',(-0.711979844231334,0.,0.702199901316089));
#26660=DIRECTION('',(0.,-1.,0.));
#26661=DIRECTION('center_axis',(0.,-1.,0.));
#26662=DIRECTION('ref_axis',(-0.711979844231334,0.,0.702199901316089));
#26663=DIRECTION('center_axis',(1.,0.,-2.53764096072769E-16));
#26664=DIRECTION('ref_axis',(2.53764096072769E-16,0.,1.));
#26665=DIRECTION('',(2.53764096072769E-16,0.,1.));
#26666=DIRECTION('',(0.,-1.,0.));
#26667=DIRECTION('',(-2.53764096072769E-16,0.,-1.));
#26668=DIRECTION('center_axis',(0.,-1.,0.));
#26669=DIRECTION('ref_axis',(-1.,0.,1.71714482808377E-14));
#26670=DIRECTION('center_axis',(0.,1.,0.));
#26671=DIRECTION('ref_axis',(-1.,0.,1.71714482808377E-14));
#26672=DIRECTION('',(0.,-1.,0.));
#26673=DIRECTION('center_axis',(0.,-1.,0.));
#26674=DIRECTION('ref_axis',(-1.,0.,1.71714482808377E-14));
#26675=DIRECTION('center_axis',(0.709478283082607,0.,0.704727298913669));
#26676=DIRECTION('ref_axis',(-0.704727298913669,0.,0.709478283082607));
#26677=DIRECTION('',(-0.704727298913669,0.,0.709478283082607));
#26678=DIRECTION('',(0.,-1.,0.));
#26679=DIRECTION('',(0.704727298913669,0.,-0.709478283082607));
#26680=DIRECTION('center_axis',(0.,-1.,0.));
#26681=DIRECTION('ref_axis',(1.,0.,-4.29093873107336E-15));
#26682=DIRECTION('center_axis',(0.,-1.,0.));
#26683=DIRECTION('ref_axis',(1.,0.,-4.29093873107336E-15));
#26684=DIRECTION('',(0.,-1.,0.));
#26685=DIRECTION('center_axis',(0.,1.,0.));
#26686=DIRECTION('ref_axis',(1.,0.,-4.29093873107336E-15));
#26687=DIRECTION('center_axis',(1.,0.,-2.53764096072769E-16));
#26688=DIRECTION('ref_axis',(2.53764096072769E-16,0.,1.));
#26689=DIRECTION('',(2.53764096072769E-16,0.,1.));
#26690=DIRECTION('',(0.,-1.,0.));
#26691=DIRECTION('',(-2.53764096072769E-16,0.,-1.));
#26692=DIRECTION('center_axis',(0.707376432457449,0.,-0.706837027046385));
#26693=DIRECTION('ref_axis',(0.706837027046385,0.,0.707376432457449));
#26694=DIRECTION('',(0.706837027046385,0.,0.707376432457449));
#26695=DIRECTION('',(0.,-1.,0.));
#26696=DIRECTION('',(-0.706837027046385,0.,-0.707376432457449));
#26697=DIRECTION('center_axis',(0.,1.,0.));
#26698=DIRECTION('ref_axis',(1.,0.,0.));
#26699=DIRECTION('',(1.,0.,-2.53764096072769E-16));
#26700=DIRECTION('',(1.,0.,0.));
#26701=DIRECTION('',(0.706837027046385,0.,-0.707376432457449));
#26702=DIRECTION('',(0.,0.,-1.));
#26703=DIRECTION('center_axis',(0.,-1.,0.));
#26704=DIRECTION('ref_axis',(-1.,0.,-4.03717463500059E-15));
#26705=DIRECTION('',(-0.704727298913669,0.,-0.709478283082607));
#26706=DIRECTION('center_axis',(0.,1.,0.));
#26707=DIRECTION('ref_axis',(1.,0.,1.69176841847649E-14));
#26708=DIRECTION('',(0.,0.,-1.));
#26709=DIRECTION('center_axis',(0.,1.,0.));
#26710=DIRECTION('ref_axis',(0.711979844231334,0.,0.702199901316089));
#26711=DIRECTION('',(0.702199901316083,0.,-0.71197984423134));
#26712=DIRECTION('center_axis',(0.,-1.,0.));
#26713=DIRECTION('ref_axis',(-0.711979844231348,0.,-0.702199901316075));
#26714=DIRECTION('center_axis',(0.,1.,0.));
#26715=DIRECTION('ref_axis',(0.245760053518569,0.,0.969330694909921));
#26716=DIRECTION('center_axis',(0.,-1.,0.));
#26717=DIRECTION('ref_axis',(-0.245760053518537,0.,-0.969330694909929));
#26718=DIRECTION('',(0.,0.,-1.));
#26719=DIRECTION('center_axis',(0.,-1.,0.));
#26720=DIRECTION('ref_axis',(-1.,0.,0.));
#26721=DIRECTION('center_axis',(0.,1.,0.));
#26722=DIRECTION('ref_axis',(0.963381374692978,0.,-0.268134904282653));
#26723=DIRECTION('center_axis',(0.,-1.,0.));
#26724=DIRECTION('ref_axis',(-0.963381374692954,0.,0.268134904282739));
#26725=DIRECTION('',(-0.703465658964221,0.,-0.710729249896213));
#26726=DIRECTION('center_axis',(0.710729249896213,0.,-0.703465658964221));
#26727=DIRECTION('ref_axis',(0.703465658964221,0.,0.710729249896213));
#26728=DIRECTION('',(0.,1.,0.));
#26729=DIRECTION('',(0.,-1.,0.));
#26730=DIRECTION('',(0.703465658964221,0.,0.710729249896213));
#26731=DIRECTION('center_axis',(0.,1.,0.));
#26732=DIRECTION('ref_axis',(-0.963381374692954,0.,0.268134904282739));
#26733=DIRECTION('',(0.,-1.,0.));
#26734=DIRECTION('center_axis',(0.,1.,0.));
#26735=DIRECTION('ref_axis',(-0.963381374692954,0.,0.268134904282739));
#26736=DIRECTION('center_axis',(0.,1.,0.));
#26737=DIRECTION('ref_axis',(0.963381374692978,0.,-0.268134904282653));
#26738=DIRECTION('',(0.,-1.,0.));
#26739=DIRECTION('center_axis',(0.,-1.,0.));
#26740=DIRECTION('ref_axis',(0.963381374692978,0.,-0.268134904282653));
#26741=DIRECTION('center_axis',(0.,1.,0.));
#26742=DIRECTION('ref_axis',(-1.,0.,0.));
#26743=DIRECTION('',(0.,-1.,0.));
#26744=DIRECTION('center_axis',(0.,1.,0.));
#26745=DIRECTION('ref_axis',(-1.,0.,0.));
#26746=DIRECTION('center_axis',(1.,0.,0.));
#26747=DIRECTION('ref_axis',(0.,0.,1.));
#26748=DIRECTION('',(0.,-1.,0.));
#26749=DIRECTION('',(0.,0.,1.));
#26750=DIRECTION('center_axis',(0.,1.,0.));
#26751=DIRECTION('ref_axis',(-0.245760053518537,0.,-0.969330694909929));
#26752=DIRECTION('',(0.,-1.,0.));
#26753=DIRECTION('center_axis',(0.,1.,0.));
#26754=DIRECTION('ref_axis',(-0.245760053518537,0.,-0.969330694909929));
#26755=DIRECTION('center_axis',(0.,1.,0.));
#26756=DIRECTION('ref_axis',(0.245760053518569,0.,0.969330694909921));
#26757=DIRECTION('',(0.,-1.,0.));
#26758=DIRECTION('center_axis',(0.,-1.,0.));
#26759=DIRECTION('ref_axis',(0.245760053518569,0.,0.969330694909921));
#26760=DIRECTION('center_axis',(0.,1.,0.));
#26761=DIRECTION('ref_axis',(-0.711979844231348,0.,-0.702199901316075));
#26762=DIRECTION('',(0.,-1.,0.));
#26763=DIRECTION('center_axis',(0.,1.,0.));
#26764=DIRECTION('ref_axis',(-0.711979844231348,0.,-0.702199901316075));
#26765=DIRECTION('center_axis',(0.71197984423134,0.,0.702199901316083));
#26766=DIRECTION('ref_axis',(-0.702199901316083,0.,0.71197984423134));
#26767=DIRECTION('',(0.,-1.,0.));
#26768=DIRECTION('',(-0.702199901316083,0.,0.71197984423134));
#26769=DIRECTION('center_axis',(0.,1.,0.));
#26770=DIRECTION('ref_axis',(0.711979844231334,0.,0.702199901316089));
#26771=DIRECTION('',(0.,-1.,0.));
#26772=DIRECTION('center_axis',(0.,-1.,0.));
#26773=DIRECTION('ref_axis',(0.711979844231334,0.,0.702199901316089));
#26774=DIRECTION('center_axis',(1.,0.,0.));
#26775=DIRECTION('ref_axis',(0.,0.,1.));
#26776=DIRECTION('',(0.,-1.,0.));
#26777=DIRECTION('',(0.,0.,1.));
#26778=DIRECTION('center_axis',(0.,1.,0.));
#26779=DIRECTION('ref_axis',(1.,0.,1.69176841847649E-14));
#26780=DIRECTION('',(0.,-1.,0.));
#26781=DIRECTION('center_axis',(0.,-1.,0.));
#26782=DIRECTION('ref_axis',(1.,0.,1.69176841847649E-14));
#26783=DIRECTION('center_axis',(0.709478283082607,0.,-0.704727298913669));
#26784=DIRECTION('ref_axis',(0.704727298913669,0.,0.709478283082607));
#26785=DIRECTION('',(0.,-1.,0.));
#26786=DIRECTION('',(0.704727298913669,0.,0.709478283082607));
#26787=DIRECTION('center_axis',(0.,1.,0.));
#26788=DIRECTION('ref_axis',(-1.,0.,-4.03717463500059E-15));
#26789=DIRECTION('',(0.,-1.,0.));
#26790=DIRECTION('center_axis',(0.,1.,0.));
#26791=DIRECTION('ref_axis',(-1.,0.,-4.03717463500059E-15));
#26792=DIRECTION('center_axis',(1.,0.,0.));
#26793=DIRECTION('ref_axis',(0.,0.,1.));
#26794=DIRECTION('',(0.,-1.,0.));
#26795=DIRECTION('',(0.,0.,1.));
#26796=DIRECTION('center_axis',(0.707376432457449,0.,0.706837027046385));
#26797=DIRECTION('ref_axis',(-0.706837027046385,0.,0.707376432457449));
#26798=DIRECTION('',(0.,-1.,0.));
#26799=DIRECTION('',(-0.706837027046385,0.,0.707376432457449));
#26800=DIRECTION('center_axis',(0.,0.,1.));
#26801=DIRECTION('ref_axis',(-1.,0.,0.));
#26802=DIRECTION('',(1.,0.,-2.53764096072769E-16));
#26803=DIRECTION('center_axis',(0.,0.,-1.));
#26804=DIRECTION('ref_axis',(1.,0.,0.));
#26805=DIRECTION('',(1.,0.,0.));
#26806=DIRECTION('center_axis',(0.,1.,0.));
#26807=DIRECTION('ref_axis',(1.,0.,0.));
#47817=CARTESIAN_POINT('',(0.,0.,0.));
#47818=CARTESIAN_POINT('Origin',(142.5822836287,255.,47.007169160326));
#47819=CARTESIAN_POINT('',(142.094409841973,15.,47.5000804575095));
#47820=CARTESIAN_POINT('',(142.094409841973,495.,47.5000804575095));
#47821=CARTESIAN_POINT('',(142.094409841973,255.,47.5000804575095));
#47822=CARTESIAN_POINT('',(142.5822836287,15.,47.007169160326));
#47823=CARTESIAN_POINT('',(142.094409841973,15.,47.5000804575095));
#47824=CARTESIAN_POINT('',(142.5822836287,495.,47.007169160326));
#47825=CARTESIAN_POINT('',(142.5822836287,255.,47.007169160326));
#47826=CARTESIAN_POINT('',(142.094409841973,495.,47.5000804575095));
#47827=CARTESIAN_POINT('Origin',(142.262455466246,255.,46.690609613792));
#47828=CARTESIAN_POINT('',(142.695977084858,15.,46.8112703207193));
#47829=CARTESIAN_POINT('Origin',(142.262455466246,15.,46.690609613792));
#47830=CARTESIAN_POINT('',(142.695977084858,495.,46.8112703207193));
#47831=CARTESIAN_POINT('',(142.695977084858,255.,46.8112703207193));
#47832=CARTESIAN_POINT('Origin',(142.262455466246,495.,46.690609613792));
#47833=CARTESIAN_POINT('Origin',(145.073060872192,255.,47.4728765656934));
#47834=CARTESIAN_POINT('',(144.344825886597,15.,45.1153516005764));
#47835=CARTESIAN_POINT('Origin',(145.073060872192,15.,47.4728765656934));
#47836=CARTESIAN_POINT('',(144.344825886597,495.,45.1153516005764));
#47837=CARTESIAN_POINT('',(144.344825886597,255.,45.1153516005764));
#47838=CARTESIAN_POINT('Origin',(145.073060872192,495.,47.4728765656934));
#47839=CARTESIAN_POINT('Origin',(144.130850755256,255.,44.4226470147914));
#47840=CARTESIAN_POINT('',(144.855850755256,15.,44.4226470147914));
#47841=CARTESIAN_POINT('Origin',(144.130850755256,15.,44.4226470147914));
#47842=CARTESIAN_POINT('',(144.855850755256,495.,44.4226470147914));
#47843=CARTESIAN_POINT('',(144.855850755256,255.,44.4226470147914));
#47844=CARTESIAN_POINT('Origin',(144.130850755256,495.,44.4226470147914));
#47845=CARTESIAN_POINT('Origin',(144.855850755256,255.,43.5036225521864));
#47846=CARTESIAN_POINT('',(144.855850755256,15.,43.5036225521864));
#47847=CARTESIAN_POINT('',(144.855850755256,15.,44.4226470147914));
#47848=CARTESIAN_POINT('',(144.855850755256,495.,43.5036225521864));
#47849=CARTESIAN_POINT('',(144.855850755256,255.,43.5036225521864));
#47850=CARTESIAN_POINT('',(144.855850755256,495.,44.4226470147914));
#47851=CARTESIAN_POINT('Origin',(144.255850755256,255.,43.5036225521863));
#47852=CARTESIAN_POINT('',(144.403306787367,15.,42.9220241352404));
#47853=CARTESIAN_POINT('Origin',(144.255850755256,15.,43.5036225521863));
#47854=CARTESIAN_POINT('',(144.403306787367,495.,42.9220241352404));
#47855=CARTESIAN_POINT('',(144.403306787367,255.,42.9220241352404));
#47856=CARTESIAN_POINT('Origin',(144.255850755256,495.,43.5036225521863));
#47857=CARTESIAN_POINT('Origin',(144.984289187873,255.,40.6305041508116));
#47858=CARTESIAN_POINT('',(142.734368503612,15.,41.3560806824536));
#47859=CARTESIAN_POINT('Origin',(144.984289187873,15.,40.6305041508116));
#47860=CARTESIAN_POINT('',(142.734368503612,495.,41.3560806824536));
#47861=CARTESIAN_POINT('',(142.734368503612,255.,41.3560806824536));
#47862=CARTESIAN_POINT('Origin',(144.984289187873,495.,40.6305041508116));
#47863=CARTESIAN_POINT('Origin',(141.401941087198,255.,41.7857749691141));
#47864=CARTESIAN_POINT('',(142.398712869122,15.,40.8026951072716));
#47865=CARTESIAN_POINT('Origin',(141.401941087198,15.,41.7857749691141));
#47866=CARTESIAN_POINT('',(142.398712869122,495.,40.8026951072716));
#47867=CARTESIAN_POINT('',(142.398712869122,255.,40.8026951072716));
#47868=CARTESIAN_POINT('Origin',(141.401941087198,495.,41.7857749691141));
#47869=CARTESIAN_POINT('Origin',(141.760942367476,255.,40.1560420081102));
#47870=CARTESIAN_POINT('',(141.760942367476,15.,40.1560420081102));
#47871=CARTESIAN_POINT('',(141.760942367476,15.,40.1560420081102));
#47872=CARTESIAN_POINT('',(141.760942367476,495.,40.1560420081102));
#47873=CARTESIAN_POINT('',(141.760942367476,255.,40.1560420081102));
#47874=CARTESIAN_POINT('',(141.760942367476,495.,40.1560420081102));
#47875=CARTESIAN_POINT('Origin',(142.508521203919,255.,39.4187321117283));
#47876=CARTESIAN_POINT('',(141.458521203919,15.,39.4187321117283));
#47877=CARTESIAN_POINT('Origin',(142.508521203919,15.,39.4187321117283));
#47878=CARTESIAN_POINT('',(141.458521203919,495.,39.4187321117283));
#47879=CARTESIAN_POINT('',(141.458521203919,255.,39.4187321117283));
#47880=CARTESIAN_POINT('Origin',(142.508521203919,495.,39.4187321117283));
#47881=CARTESIAN_POINT('Origin',(141.458521203919,255.,37.9151793916432));
#47882=CARTESIAN_POINT('',(141.458521203919,15.,37.9151793916432));
#47883=CARTESIAN_POINT('',(141.458521203919,15.,39.4187321117283));
#47884=CARTESIAN_POINT('',(141.458521203919,495.,37.9151793916432));
#47885=CARTESIAN_POINT('',(141.458521203919,255.,37.9151793916432));
#47886=CARTESIAN_POINT('',(141.458521203919,495.,39.4187321117283));
#47887=CARTESIAN_POINT('Origin',(142.508521203919,255.,37.9151793916432));
#47888=CARTESIAN_POINT('',(141.763569006683,15.,37.1752157277839));
#47889=CARTESIAN_POINT('Origin',(142.508521203919,15.,37.9151793916432));
#47890=CARTESIAN_POINT('',(141.763569006683,495.,37.1752157277839));
#47891=CARTESIAN_POINT('',(141.763569006683,255.,37.1752157277839));
#47892=CARTESIAN_POINT('Origin',(142.508521203919,495.,37.9151793916432));
#47893=CARTESIAN_POINT('Origin',(144.544688744748,255.,34.375346814161));
#47894=CARTESIAN_POINT('',(144.544688744748,15.,34.375346814161));
#47895=CARTESIAN_POINT('',(144.544688744748,15.,34.375346814161));
#47896=CARTESIAN_POINT('',(144.544688744748,495.,34.375346814161));
#47897=CARTESIAN_POINT('',(144.544688744748,255.,34.375346814161));
#47898=CARTESIAN_POINT('',(144.544688744748,495.,34.375346814161));
#47899=CARTESIAN_POINT('Origin',(143.764262633357,255.,33.6001467853559));
#47900=CARTESIAN_POINT('',(144.864262633357,15.,33.6001467853559));
#47901=CARTESIAN_POINT('Origin',(143.764262633357,15.,33.6001467853559));
#47902=CARTESIAN_POINT('',(144.864262633357,495.,33.6001467853559));
#47903=CARTESIAN_POINT('',(144.864262633357,255.,33.6001467853559));
#47904=CARTESIAN_POINT('Origin',(143.764262633357,495.,33.6001467853559));
#47905=CARTESIAN_POINT('Origin',(144.864262633357,255.,31.0022770426652));
#47906=CARTESIAN_POINT('',(144.864262633357,15.,31.0022770426652));
#47907=CARTESIAN_POINT('',(144.864262633357,15.,31.0022770426652));
#47908=CARTESIAN_POINT('',(144.864262633357,495.,31.0022770426652));
#47909=CARTESIAN_POINT('',(144.864262633357,255.,31.0022770426652));
#47910=CARTESIAN_POINT('',(144.864262633357,495.,31.0022770426652));
#47911=CARTESIAN_POINT('Origin',(143.862749870693,255.,30.));
#47912=CARTESIAN_POINT('',(143.862749870693,15.,30.));
#47913=CARTESIAN_POINT('',(143.862749870693,15.,30.));
#47914=CARTESIAN_POINT('',(143.862749870693,495.,30.));
#47915=CARTESIAN_POINT('',(143.862749870693,255.,30.));
#47916=CARTESIAN_POINT('',(143.862749870693,495.,30.));
#47917=CARTESIAN_POINT('Origin',(129.866920906812,495.,38.7500402287547));
#47918=CARTESIAN_POINT('',(127.637659789347,495.,47.5000804575095));
#47919=CARTESIAN_POINT('',(144.864262633357,495.,47.5000804575095));
#47920=CARTESIAN_POINT('',(125.869319760628,495.,30.));
#47921=CARTESIAN_POINT('',(144.864262633357,495.,30.));
#47922=CARTESIAN_POINT('',(124.867806997963,495.,31.0022770426652));
#47923=CARTESIAN_POINT('',(125.869319760628,495.,30.));
#47924=CARTESIAN_POINT('',(124.867806997963,495.,33.6001467853559));
#47925=CARTESIAN_POINT('',(124.867806997963,495.,31.0022770426652));
#47926=CARTESIAN_POINT('',(125.187380886572,495.,34.375346814161));
#47927=CARTESIAN_POINT('Origin',(125.967806997963,495.,33.6001467853559));
#47928=CARTESIAN_POINT('',(127.968500624638,495.,37.1752157277839));
#47929=CARTESIAN_POINT('',(125.187380886572,495.,34.375346814161));
#47930=CARTESIAN_POINT('',(128.273548427401,495.,37.9151793916432));
#47931=CARTESIAN_POINT('Origin',(127.223548427401,495.,37.9151793916432));
#47932=CARTESIAN_POINT('',(128.273548427401,495.,39.4187321117283));
#47933=CARTESIAN_POINT('',(128.273548427401,495.,39.4187321117283));
#47934=CARTESIAN_POINT('',(127.971127263844,495.,40.1560420081102));
#47935=CARTESIAN_POINT('Origin',(127.223548427401,495.,39.4187321117283));
#47936=CARTESIAN_POINT('',(127.333356762198,495.,40.8026951072716));
#47937=CARTESIAN_POINT('',(127.971127263844,495.,40.1560420081102));
#47938=CARTESIAN_POINT('',(126.997701127708,495.,41.3560806824536));
#47939=CARTESIAN_POINT('Origin',(128.330128544122,495.,41.7857749691141));
#47940=CARTESIAN_POINT('',(125.328762843953,495.,42.9220241352404));
#47941=CARTESIAN_POINT('Origin',(124.747780443448,495.,40.6305041508116));
#47942=CARTESIAN_POINT('',(124.876218876064,495.,43.5036225521864));
#47943=CARTESIAN_POINT('Origin',(125.476218876064,495.,43.5036225521863));
#47944=CARTESIAN_POINT('',(124.876218876064,495.,44.4226470147914));
#47945=CARTESIAN_POINT('',(124.876218876064,495.,44.4226470147914));
#47946=CARTESIAN_POINT('',(125.387243744723,495.,45.1153516005764));
#47947=CARTESIAN_POINT('Origin',(125.601218876064,495.,44.4226470147914));
#47948=CARTESIAN_POINT('',(127.036092546462,495.,46.8112703207193));
#47949=CARTESIAN_POINT('Origin',(124.659008759128,495.,47.4728765656934));
#47950=CARTESIAN_POINT('',(127.149786002621,495.,47.007169160326));
#47951=CARTESIAN_POINT('Origin',(127.469614165074,495.,46.690609613792));
#47952=CARTESIAN_POINT('',(127.637659789347,495.,47.5000804575095));
#47953=CARTESIAN_POINT('Origin',(127.149786002621,255.,47.007169160326));
#47954=CARTESIAN_POINT('',(127.637659789347,15.,47.5000804575095));
#47955=CARTESIAN_POINT('',(127.637659789347,255.,47.5000804575095));
#47956=CARTESIAN_POINT('',(127.149786002621,15.,47.007169160326));
#47957=CARTESIAN_POINT('',(127.149786002621,255.,47.007169160326));
#47958=CARTESIAN_POINT('',(127.637659789347,15.,47.5000804575095));
#47959=CARTESIAN_POINT('Origin',(127.469614165074,255.,46.690609613792));
#47960=CARTESIAN_POINT('',(127.036092546462,15.,46.8112703207193));
#47961=CARTESIAN_POINT('',(127.036092546462,255.,46.8112703207193));
#47962=CARTESIAN_POINT('Origin',(127.469614165074,15.,46.690609613792));
#47963=CARTESIAN_POINT('Origin',(124.659008759128,255.,47.4728765656934));
#47964=CARTESIAN_POINT('',(125.387243744723,15.,45.1153516005764));
#47965=CARTESIAN_POINT('',(125.387243744723,255.,45.1153516005764));
#47966=CARTESIAN_POINT('Origin',(124.659008759128,15.,47.4728765656934));
#47967=CARTESIAN_POINT('Origin',(125.601218876064,255.,44.4226470147914));
#47968=CARTESIAN_POINT('',(124.876218876064,15.,44.4226470147914));
#47969=CARTESIAN_POINT('',(124.876218876064,255.,44.4226470147914));
#47970=CARTESIAN_POINT('Origin',(125.601218876064,15.,44.4226470147914));
#47971=CARTESIAN_POINT('Origin',(124.876218876064,255.,43.5036225521864));
#47972=CARTESIAN_POINT('',(124.876218876064,15.,43.5036225521864));
#47973=CARTESIAN_POINT('',(124.876218876064,255.,43.5036225521864));
#47974=CARTESIAN_POINT('',(124.876218876064,15.,44.4226470147914));
#47975=CARTESIAN_POINT('Origin',(125.476218876064,255.,43.5036225521863));
#47976=CARTESIAN_POINT('',(125.328762843953,15.,42.9220241352404));
#47977=CARTESIAN_POINT('',(125.328762843953,255.,42.9220241352404));
#47978=CARTESIAN_POINT('Origin',(125.476218876064,15.,43.5036225521863));
#47979=CARTESIAN_POINT('Origin',(124.747780443448,255.,40.6305041508116));
#47980=CARTESIAN_POINT('',(126.997701127708,15.,41.3560806824536));
#47981=CARTESIAN_POINT('',(126.997701127708,255.,41.3560806824536));
#47982=CARTESIAN_POINT('Origin',(124.747780443448,15.,40.6305041508116));
#47983=CARTESIAN_POINT('Origin',(128.330128544122,255.,41.7857749691141));
#47984=CARTESIAN_POINT('',(127.333356762198,15.,40.8026951072716));
#47985=CARTESIAN_POINT('',(127.333356762198,255.,40.8026951072716));
#47986=CARTESIAN_POINT('Origin',(128.330128544122,15.,41.7857749691141));
#47987=CARTESIAN_POINT('Origin',(127.971127263844,255.,40.1560420081102));
#47988=CARTESIAN_POINT('',(127.971127263844,15.,40.1560420081102));
#47989=CARTESIAN_POINT('',(127.971127263844,255.,40.1560420081102));
#47990=CARTESIAN_POINT('',(127.971127263844,15.,40.1560420081102));
#47991=CARTESIAN_POINT('Origin',(127.223548427401,255.,39.4187321117283));
#47992=CARTESIAN_POINT('',(128.273548427401,15.,39.4187321117283));
#47993=CARTESIAN_POINT('',(128.273548427401,255.,39.4187321117283));
#47994=CARTESIAN_POINT('Origin',(127.223548427401,15.,39.4187321117283));
#47995=CARTESIAN_POINT('Origin',(128.273548427401,255.,37.9151793916432));
#47996=CARTESIAN_POINT('',(128.273548427401,15.,37.9151793916432));
#47997=CARTESIAN_POINT('',(128.273548427401,255.,37.9151793916432));
#47998=CARTESIAN_POINT('',(128.273548427401,15.,39.4187321117283));
#47999=CARTESIAN_POINT('Origin',(127.223548427401,255.,37.9151793916432));
#48000=CARTESIAN_POINT('',(127.968500624638,15.,37.1752157277839));
#48001=CARTESIAN_POINT('',(127.968500624638,255.,37.1752157277839));
#48002=CARTESIAN_POINT('Origin',(127.223548427401,15.,37.9151793916432));
#48003=CARTESIAN_POINT('Origin',(125.187380886572,255.,34.375346814161));
#48004=CARTESIAN_POINT('',(125.187380886572,15.,34.375346814161));
#48005=CARTESIAN_POINT('',(125.187380886572,255.,34.375346814161));
#48006=CARTESIAN_POINT('',(125.187380886572,15.,34.375346814161));
#48007=CARTESIAN_POINT('Origin',(125.967806997963,255.,33.6001467853559));
#48008=CARTESIAN_POINT('',(124.867806997963,15.,33.6001467853559));
#48009=CARTESIAN_POINT('',(124.867806997963,255.,33.6001467853559));
#48010=CARTESIAN_POINT('Origin',(125.967806997963,15.,33.6001467853559));
#48011=CARTESIAN_POINT('Origin',(124.867806997963,255.,31.0022770426652));
#48012=CARTESIAN_POINT('',(124.867806997963,15.,31.0022770426652));
#48013=CARTESIAN_POINT('',(124.867806997963,255.,31.0022770426652));
#48014=CARTESIAN_POINT('',(124.867806997963,15.,31.0022770426652));
#48015=CARTESIAN_POINT('Origin',(125.869319760628,255.,30.));
#48016=CARTESIAN_POINT('',(125.869319760628,15.,30.));
#48017=CARTESIAN_POINT('',(125.869319760628,255.,30.));
#48018=CARTESIAN_POINT('',(125.869319760628,15.,30.));
#48019=CARTESIAN_POINT('Origin',(134.86603481566,255.,30.));
#48020=CARTESIAN_POINT('',(124.867806997963,15.,30.));
#48021=CARTESIAN_POINT('Origin',(127.637659789347,255.,47.5000804575095));
#48022=CARTESIAN_POINT('',(124.867806997963,15.,47.5000804575095));
#48023=CARTESIAN_POINT('Origin',(129.866920906812,15.,38.7500402287547));
#48351=UNCERTAINTY_MEASURE_WITH_UNIT(LENGTH_MEASURE(0.01),#48370,
'DISTANCE_ACCURACY_VALUE',
'Maximum model space distance between geometric entities at asserted c
onnectivities');
#48356=UNCERTAINTY_MEASURE_WITH_UNIT(LENGTH_MEASURE(0.01),#48370,
'DISTANCE_ACCURACY_VALUE',
'Maximum model space distance between geometric entities at asserted c
onnectivities');
#48364=(
GEOMETRIC_REPRESENTATION_CONTEXT(3)
GLOBAL_UNCERTAINTY_ASSIGNED_CONTEXT((#48351))
GLOBAL_UNIT_ASSIGNED_CONTEXT((#48370,#48372,#48373))
REPRESENTATION_CONTEXT('','3D')
);
#48369=(
GEOMETRIC_REPRESENTATION_CONTEXT(3)
GLOBAL_UNCERTAINTY_ASSIGNED_CONTEXT((#48356))
GLOBAL_UNIT_ASSIGNED_CONTEXT((#48370,#48372,#48373))
REPRESENTATION_CONTEXT('','3D')
);
#48370=(
LENGTH_UNIT()
NAMED_UNIT(*)
SI_UNIT(.MILLI.,.METRE.)
);
#48372=(
NAMED_UNIT(*)
PLANE_ANGLE_UNIT()
SI_UNIT($,.RADIAN.)
);
#48373=(
NAMED_UNIT(*)
SI_UNIT($,.STERADIAN.)
SOLID_ANGLE_UNIT()
);
#48381=SHAPE_DEFINITION_REPRESENTATION(#48393,#48419);
#48393=PRODUCT_DEFINITION_SHAPE('',$,#48432);
#48419=SHAPE_REPRESENTATION('',(#21736),#48364);
#48424=PRODUCT_DEFINITION_CONTEXT('part definition',#48462,'design');
#48432=PRODUCT_DEFINITION('Rail_02','Rail_02',#48444,#48424);
#48444=PRODUCT_DEFINITION_FORMATION('',$,#48471);
#48462=APPLICATION_CONTEXT(
'Core Data for Automotive Mechanical Design Process');
#48463=PRODUCT_CONTEXT('part definition',#48462,'mechanical');
#48471=PRODUCT('Rail_02','Rail_02',$,(#48463));
#48525=COLOUR_RGB('Off White',0.89,0.88,0.83);
#48526=FILL_AREA_STYLE_COLOUR('',#48525);
#48527=FILL_AREA_STYLE('',(#48526));
#48528=SURFACE_STYLE_FILL_AREA(#48527);
#48529=SURFACE_SIDE_STYLE('',(#48528));
#48530=SURFACE_STYLE_USAGE(.BOTH.,#48529);
#48531=PRESENTATION_STYLE_ASSIGNMENT((#48530));
ENDSEC;
END-ISO-10303-21;
